ISO-10303-21;
HEADER;
/* Generated by software containing ST-Developer
 * from STEP Tools, Inc. (www.steptools.com) 
 */

FILE_DESCRIPTION(
/* description */ ('PAT-096'),
/* implementation_level */ '2;1');

FILE_NAME(
/* name */ 'Cap Screw - M4x16.step',
/* time_stamp */ '2026-10-29T17:03:14-07:00',
/* author */ (''),
/* organization */ (''),
/* preprocessor_version */ 'ST-DEVELOPER v20.2',
/* originating_system */ 'Autodesk Translation Framework v15.17.0.0',
/* authorisation */ '');

FILE_SCHEMA (('AUTOMOTIVE_DESIGN { 1 0 10303 214 3 1 1 }'));
ENDSEC;

DATA;
#10=MECHANICAL_DESIGN_GEOMETRIC_PRESENTATION_REPRESENTATION('',(#422),#10650);
#322=CONICAL_SURFACE('',#6353,0.325,0.785398163397448);
#323=CONICAL_SURFACE('',#6357,0.335,0.785398163397448);
#324=CONICAL_SURFACE('',#6361,0.21,0.463647609000806);
#325=CONICAL_SURFACE('',#6365,0.18,0.785398163397448);
#331=ORIENTED_CLOSED_SHELL('',*,#5557,.F.);
#334=BREP_WITH_VOIDS('Body1',#5556,(#331));
#352=SHAPE_REPRESENTATION_RELATIONSHIP('SRR','None',#10814,#383);
#383=ADVANCED_BREP_SHAPE_REPRESENTATION('',(#334),#10632);
#422=STYLED_ITEM('',(#11071),#334);
#557=FACE_BOUND('',#1412,.T.);
#705=PLANE('',#6351);
#706=PLANE('',#6359);
#707=PLANE('',#6367);
#708=PLANE('',#6368);
#709=PLANE('',#6369);
#710=PLANE('',#6370);
#711=PLANE('',#6371);
#712=PLANE('',#6372);
#713=PLANE('',#6373);
#714=PLANE('',#6374);
#715=PLANE('',#6375);
#987=FACE_OUTER_BOUND('',#1407,.T.);
#988=FACE_OUTER_BOUND('',#1408,.T.);
#989=FACE_OUTER_BOUND('',#1409,.T.);
#990=FACE_OUTER_BOUND('',#1410,.T.);
#991=FACE_OUTER_BOUND('',#1411,.T.);
#992=FACE_OUTER_BOUND('',#1413,.T.);
#993=FACE_OUTER_BOUND('',#1414,.T.);
#994=FACE_OUTER_BOUND('',#1415,.T.);
#995=FACE_OUTER_BOUND('',#1416,.T.);
#996=FACE_OUTER_BOUND('',#1417,.T.);
#997=FACE_OUTER_BOUND('',#1418,.T.);
#998=FACE_OUTER_BOUND('',#1419,.T.);
#999=FACE_OUTER_BOUND('',#1420,.T.);
#1000=FACE_OUTER_BOUND('',#1421,.T.);
#1001=FACE_OUTER_BOUND('',#1422,.T.);
#1002=FACE_OUTER_BOUND('',#1423,.T.);
#1003=FACE_OUTER_BOUND('',#1424,.T.);
#1407=EDGE_LOOP('',(#4549));
#1408=EDGE_LOOP('',(#4550,#4551,#4552,#4553));
#1409=EDGE_LOOP('',(#4554,#4555,#4556,#4557));
#1410=EDGE_LOOP('',(#4558,#4559,#4560,#4561));
#1411=EDGE_LOOP('',(#4562));
#1412=EDGE_LOOP('',(#4563));
#1413=EDGE_LOOP('',(#4564,#4565,#4566,#4567));
#1414=EDGE_LOOP('',(#4568,#4569,#4570,#4571));
#1415=EDGE_LOOP('',(#4572,#4573,#4574,#4575));
#1416=EDGE_LOOP('',(#4576));
#1417=EDGE_LOOP('',(#4577,#4578,#4579,#4580));
#1418=EDGE_LOOP('',(#4581,#4582,#4583,#4584));
#1419=EDGE_LOOP('',(#4585,#4586,#4587,#4588));
#1420=EDGE_LOOP('',(#4589,#4590,#4591,#4592));
#1421=EDGE_LOOP('',(#4593,#4594,#4595,#4596));
#1422=EDGE_LOOP('',(#4597,#4598,#4599,#4600));
#1423=EDGE_LOOP('',(#4601,#4602,#4603,#4604,#4605,#4606));
#1424=EDGE_LOOP('',(#4607,#4608,#4609,#4610,#4611,#4612));
#1774=LINE('',#9931,#2103);
#1775=LINE('',#9935,#2104);
#1776=LINE('',#9939,#2105);
#1777=LINE('',#9946,#2106);
#1778=LINE('',#9950,#2107);
#1779=LINE('',#9954,#2108);
#1780=LINE('',#9959,#2109);
#1781=LINE('',#9961,#2110);
#1782=LINE('',#9963,#2111);
#1783=LINE('',#9964,#2112);
#1784=LINE('',#9967,#2113);
#1785=LINE('',#9969,#2114);
#1786=LINE('',#9970,#2115);
#1787=LINE('',#9973,#2116);
#1788=LINE('',#9975,#2117);
#1789=LINE('',#9976,#2118);
#1790=LINE('',#9979,#2119);
#1791=LINE('',#9981,#2120);
#1792=LINE('',#9982,#2121);
#1793=LINE('',#9985,#2122);
#1794=LINE('',#9987,#2123);
#1795=LINE('',#9988,#2124);
#1796=LINE('',#9990,#2125);
#1797=LINE('',#9991,#2126);
#2103=VECTOR('',#7724,0.325);
#2104=VECTOR('',#7729,0.35);
#2105=VECTOR('',#7734,0.335);
#2106=VECTOR('',#7743,0.21);
#2107=VECTOR('',#7748,0.2);
#2108=VECTOR('',#7753,0.18);
#2109=VECTOR('',#7758,1.);
#2110=VECTOR('',#7759,1.);
#2111=VECTOR('',#7760,1.);
#2112=VECTOR('',#7761,1.);
#2113=VECTOR('',#7764,1.);
#2114=VECTOR('',#7765,1.);
#2115=VECTOR('',#7766,1.);
#2116=VECTOR('',#7769,1.);
#2117=VECTOR('',#7770,1.);
#2118=VECTOR('',#7771,1.);
#2119=VECTOR('',#7774,1.);
#2120=VECTOR('',#7775,1.);
#2121=VECTOR('',#7776,1.);
#2122=VECTOR('',#7779,1.);
#2123=VECTOR('',#7780,1.);
#2124=VECTOR('',#7781,1.);
#2125=VECTOR('',#7784,1.);
#2126=VECTOR('',#7785,1.);
#2472=CIRCLE('',#6352,0.3);
#2473=CIRCLE('',#6354,0.35);
#2474=CIRCLE('',#6356,0.35);
#2475=CIRCLE('',#6358,0.32);
#2476=CIRCLE('',#6360,0.22);
#2477=CIRCLE('',#6362,0.1954);
#2478=CIRCLE('',#6364,0.1954);
#2479=CIRCLE('',#6366,0.16);
#2864=VERTEX_POINT('',#9926);
#2865=VERTEX_POINT('',#9929);
#2866=VERTEX_POINT('',#9933);
#2867=VERTEX_POINT('',#9937);
#2868=VERTEX_POINT('',#9941);
#2869=VERTEX_POINT('',#9944);
#2870=VERTEX_POINT('',#9948);
#2871=VERTEX_POINT('',#9952);
#2872=VERTEX_POINT('',#9957);
#2873=VERTEX_POINT('',#9958);
#2874=VERTEX_POINT('',#9960);
#2875=VERTEX_POINT('',#9962);
#2876=VERTEX_POINT('',#9966);
#2877=VERTEX_POINT('',#9968);
#2878=VERTEX_POINT('',#9972);
#2879=VERTEX_POINT('',#9974);
#2880=VERTEX_POINT('',#9978);
#2881=VERTEX_POINT('',#9980);
#2882=VERTEX_POINT('',#9984);
#2883=VERTEX_POINT('',#9986);
#3453=EDGE_CURVE('',#2864,#2864,#2472,.T.);
#3454=EDGE_CURVE('',#2865,#2865,#2473,.T.);
#3455=EDGE_CURVE('',#2865,#2864,#1774,.T.);
#3456=EDGE_CURVE('',#2866,#2866,#2474,.T.);
#3457=EDGE_CURVE('',#2866,#2865,#1775,.T.);
#3458=EDGE_CURVE('',#2867,#2867,#2475,.T.);
#3459=EDGE_CURVE('',#2867,#2866,#1776,.T.);
#3460=EDGE_CURVE('',#2868,#2868,#2476,.T.);
#3461=EDGE_CURVE('',#2869,#2869,#2477,.F.);
#3462=EDGE_CURVE('',#2869,#2868,#1777,.T.);
#3463=EDGE_CURVE('',#2870,#2870,#2478,.F.);
#3464=EDGE_CURVE('',#2870,#2869,#1778,.T.);
#3465=EDGE_CURVE('',#2871,#2871,#2479,.T.);
#3466=EDGE_CURVE('',#2871,#2870,#1779,.T.);
#3467=EDGE_CURVE('',#2872,#2873,#1780,.T.);
#3468=EDGE_CURVE('',#2873,#2874,#1781,.T.);
#3469=EDGE_CURVE('',#2874,#2875,#1782,.T.);
#3470=EDGE_CURVE('',#2872,#2875,#1783,.T.);
#3471=EDGE_CURVE('',#2873,#2876,#1784,.T.);
#3472=EDGE_CURVE('',#2876,#2877,#1785,.T.);
#3473=EDGE_CURVE('',#2877,#2874,#1786,.T.);
#3474=EDGE_CURVE('',#2876,#2878,#1787,.T.);
#3475=EDGE_CURVE('',#2878,#2879,#1788,.T.);
#3476=EDGE_CURVE('',#2879,#2877,#1789,.T.);
#3477=EDGE_CURVE('',#2878,#2880,#1790,.T.);
#3478=EDGE_CURVE('',#2880,#2881,#1791,.T.);
#3479=EDGE_CURVE('',#2881,#2879,#1792,.T.);
#3480=EDGE_CURVE('',#2880,#2882,#1793,.T.);
#3481=EDGE_CURVE('',#2882,#2883,#1794,.T.);
#3482=EDGE_CURVE('',#2883,#2881,#1795,.T.);
#3483=EDGE_CURVE('',#2882,#2872,#1796,.T.);
#3484=EDGE_CURVE('',#2875,#2883,#1797,.T.);
#4549=ORIENTED_EDGE('',*,*,#3453,.F.);
#4550=ORIENTED_EDGE('',*,*,#3454,.F.);
#4551=ORIENTED_EDGE('',*,*,#3455,.T.);
#4552=ORIENTED_EDGE('',*,*,#3453,.T.);
#4553=ORIENTED_EDGE('',*,*,#3455,.F.);
#4554=ORIENTED_EDGE('',*,*,#3456,.F.);
#4555=ORIENTED_EDGE('',*,*,#3457,.T.);
#4556=ORIENTED_EDGE('',*,*,#3454,.T.);
#4557=ORIENTED_EDGE('',*,*,#3457,.F.);
#4558=ORIENTED_EDGE('',*,*,#3458,.F.);
#4559=ORIENTED_EDGE('',*,*,#3459,.T.);
#4560=ORIENTED_EDGE('',*,*,#3456,.T.);
#4561=ORIENTED_EDGE('',*,*,#3459,.F.);
#4562=ORIENTED_EDGE('',*,*,#3458,.T.);
#4563=ORIENTED_EDGE('',*,*,#3460,.F.);
#4564=ORIENTED_EDGE('',*,*,#3461,.F.);
#4565=ORIENTED_EDGE('',*,*,#3462,.T.);
#4566=ORIENTED_EDGE('',*,*,#3460,.T.);
#4567=ORIENTED_EDGE('',*,*,#3462,.F.);
#4568=ORIENTED_EDGE('',*,*,#3463,.F.);
#4569=ORIENTED_EDGE('',*,*,#3464,.T.);
#4570=ORIENTED_EDGE('',*,*,#3461,.T.);
#4571=ORIENTED_EDGE('',*,*,#3464,.F.);
#4572=ORIENTED_EDGE('',*,*,#3465,.F.);
#4573=ORIENTED_EDGE('',*,*,#3466,.T.);
#4574=ORIENTED_EDGE('',*,*,#3463,.T.);
#4575=ORIENTED_EDGE('',*,*,#3466,.F.);
#4576=ORIENTED_EDGE('',*,*,#3465,.T.);
#4577=ORIENTED_EDGE('',*,*,#3467,.T.);
#4578=ORIENTED_EDGE('',*,*,#3468,.T.);
#4579=ORIENTED_EDGE('',*,*,#3469,.T.);
#4580=ORIENTED_EDGE('',*,*,#3470,.F.);
#4581=ORIENTED_EDGE('',*,*,#3471,.T.);
#4582=ORIENTED_EDGE('',*,*,#3472,.T.);
#4583=ORIENTED_EDGE('',*,*,#3473,.T.);
#4584=ORIENTED_EDGE('',*,*,#3468,.F.);
#4585=ORIENTED_EDGE('',*,*,#3474,.T.);
#4586=ORIENTED_EDGE('',*,*,#3475,.T.);
#4587=ORIENTED_EDGE('',*,*,#3476,.T.);
#4588=ORIENTED_EDGE('',*,*,#3472,.F.);
#4589=ORIENTED_EDGE('',*,*,#3477,.T.);
#4590=ORIENTED_EDGE('',*,*,#3478,.T.);
#4591=ORIENTED_EDGE('',*,*,#3479,.T.);
#4592=ORIENTED_EDGE('',*,*,#3475,.F.);
#4593=ORIENTED_EDGE('',*,*,#3480,.T.);
#4594=ORIENTED_EDGE('',*,*,#3481,.T.);
#4595=ORIENTED_EDGE('',*,*,#3482,.T.);
#4596=ORIENTED_EDGE('',*,*,#3478,.F.);
#4597=ORIENTED_EDGE('',*,*,#3483,.T.);
#4598=ORIENTED_EDGE('',*,*,#3470,.T.);
#4599=ORIENTED_EDGE('',*,*,#3484,.T.);
#4600=ORIENTED_EDGE('',*,*,#3481,.F.);
#4601=ORIENTED_EDGE('',*,*,#3483,.F.);
#4602=ORIENTED_EDGE('',*,*,#3480,.F.);
#4603=ORIENTED_EDGE('',*,*,#3477,.F.);
#4604=ORIENTED_EDGE('',*,*,#3474,.F.);
#4605=ORIENTED_EDGE('',*,*,#3471,.F.);
#4606=ORIENTED_EDGE('',*,*,#3467,.F.);
#4607=ORIENTED_EDGE('',*,*,#3484,.F.);
#4608=ORIENTED_EDGE('',*,*,#3469,.F.);
#4609=ORIENTED_EDGE('',*,*,#3473,.F.);
#4610=ORIENTED_EDGE('',*,*,#3476,.F.);
#4611=ORIENTED_EDGE('',*,*,#3479,.F.);
#4612=ORIENTED_EDGE('',*,*,#3482,.F.);
#5149=CYLINDRICAL_SURFACE('',#6355,0.35);
#5150=CYLINDRICAL_SURFACE('',#6363,0.1954);
#5392=ADVANCED_FACE('',(#987),#705,.T.);
#5393=ADVANCED_FACE('',(#988),#322,.T.);
#5394=ADVANCED_FACE('',(#989),#5149,.T.);
#5395=ADVANCED_FACE('',(#990),#323,.T.);
#5396=ADVANCED_FACE('',(#991,#557),#706,.T.);
#5397=ADVANCED_FACE('',(#992),#324,.T.);
#5398=ADVANCED_FACE('',(#993),#5150,.T.);
#5399=ADVANCED_FACE('',(#994),#325,.T.);
#5400=ADVANCED_FACE('',(#995),#707,.T.);
#5401=ADVANCED_FACE('',(#996),#708,.F.);
#5402=ADVANCED_FACE('',(#997),#709,.F.);
#5403=ADVANCED_FACE('',(#998),#710,.F.);
#5404=ADVANCED_FACE('',(#999),#711,.F.);
#5405=ADVANCED_FACE('',(#1000),#712,.F.);
#5406=ADVANCED_FACE('',(#1001),#713,.F.);
#5407=ADVANCED_FACE('',(#1002),#714,.F.);
#5408=ADVANCED_FACE('',(#1003),#715,.F.);
#5556=CLOSED_SHELL('',(#5392,#5393,#5394,#5395,#5396,#5397,#5398,#5399,
#5400));
#5557=CLOSED_SHELL('',(#5401,#5402,#5403,#5404,#5405,#5406,#5407,#5408));
#6350=AXIS2_PLACEMENT_3D('',#9924,#7714,#7715);
#6351=AXIS2_PLACEMENT_3D('',#9925,#7716,#7717);
#6352=AXIS2_PLACEMENT_3D('',#9927,#7718,#7719);
#6353=AXIS2_PLACEMENT_3D('',#9928,#7720,#7721);
#6354=AXIS2_PLACEMENT_3D('',#9930,#7722,#7723);
#6355=AXIS2_PLACEMENT_3D('',#9932,#7725,#7726);
#6356=AXIS2_PLACEMENT_3D('',#9934,#7727,#7728);
#6357=AXIS2_PLACEMENT_3D('',#9936,#7730,#7731);
#6358=AXIS2_PLACEMENT_3D('',#9938,#7732,#7733);
#6359=AXIS2_PLACEMENT_3D('',#9940,#7735,#7736);
#6360=AXIS2_PLACEMENT_3D('',#9942,#7737,#7738);
#6361=AXIS2_PLACEMENT_3D('',#9943,#7739,#7740);
#6362=AXIS2_PLACEMENT_3D('',#9945,#7741,#7742);
#6363=AXIS2_PLACEMENT_3D('',#9947,#7744,#7745);
#6364=AXIS2_PLACEMENT_3D('',#9949,#7746,#7747);
#6365=AXIS2_PLACEMENT_3D('',#9951,#7749,#7750);
#6366=AXIS2_PLACEMENT_3D('',#9953,#7751,#7752);
#6367=AXIS2_PLACEMENT_3D('',#9955,#7754,#7755);
#6368=AXIS2_PLACEMENT_3D('',#9956,#7756,#7757);
#6369=AXIS2_PLACEMENT_3D('',#9965,#7762,#7763);
#6370=AXIS2_PLACEMENT_3D('',#9971,#7767,#7768);
#6371=AXIS2_PLACEMENT_3D('',#9977,#7772,#7773);
#6372=AXIS2_PLACEMENT_3D('',#9983,#7777,#7778);
#6373=AXIS2_PLACEMENT_3D('',#9989,#7782,#7783);
#6374=AXIS2_PLACEMENT_3D('',#9992,#7786,#7787);
#6375=AXIS2_PLACEMENT_3D('',#9993,#7788,#7789);
#7714=DIRECTION('axis',(0.,0.,1.));
#7715=DIRECTION('refdir',(1.,0.,0.));
#7716=DIRECTION('center_axis',(0.,1.,0.));
#7717=DIRECTION('ref_axis',(0.,0.,1.));
#7718=DIRECTION('center_axis',(0.,-1.,0.));
#7719=DIRECTION('ref_axis',(1.,0.,0.));
#7720=DIRECTION('center_axis',(0.,-1.,0.));
#7721=DIRECTION('ref_axis',(1.,0.,0.));
#7722=DIRECTION('center_axis',(0.,-1.,0.));
#7723=DIRECTION('ref_axis',(1.,0.,0.));
#7724=DIRECTION('',(0.707106781186547,0.707106781186548,8.65956056235493E-17));
#7725=DIRECTION('center_axis',(0.,-1.,0.));
#7726=DIRECTION('ref_axis',(1.,0.,0.));
#7727=DIRECTION('center_axis',(0.,-1.,0.));
#7728=DIRECTION('ref_axis',(1.,0.,0.));
#7729=DIRECTION('',(0.,1.,0.));
#7730=DIRECTION('center_axis',(0.,1.,0.));
#7731=DIRECTION('ref_axis',(1.,0.,0.));
#7732=DIRECTION('center_axis',(0.,-1.,0.));
#7733=DIRECTION('ref_axis',(1.,0.,0.));
#7734=DIRECTION('',(-0.707106781186547,0.707106781186548,-8.65956056235493E-17));
#7735=DIRECTION('center_axis',(0.,-1.,0.));
#7736=DIRECTION('ref_axis',(0.,0.,-1.));
#7737=DIRECTION('center_axis',(0.,-1.,0.));
#7738=DIRECTION('ref_axis',(1.,0.,0.));
#7739=DIRECTION('center_axis',(0.,1.,0.));
#7740=DIRECTION('ref_axis',(1.,0.,0.));
#7741=DIRECTION('center_axis',(0.,1.,0.));
#7742=DIRECTION('ref_axis',(1.,0.,0.));
#7743=DIRECTION('',(-0.447213595499958,0.894427190999916,-5.47678698264203E-17));
#7744=DIRECTION('center_axis',(0.,-1.,0.));
#7745=DIRECTION('ref_axis',(1.,0.,0.));
#7746=DIRECTION('center_axis',(0.,1.,0.));
#7747=DIRECTION('ref_axis',(1.,0.,0.));
#7748=DIRECTION('',(0.,1.,0.));
#7749=DIRECTION('center_axis',(0.,1.,0.));
#7750=DIRECTION('ref_axis',(1.,0.,0.));
#7751=DIRECTION('center_axis',(0.,-1.,0.));
#7752=DIRECTION('ref_axis',(1.,0.,0.));
#7753=DIRECTION('',(-0.707106781186547,0.707106781186548,-8.65956056235493E-17));
#7754=DIRECTION('center_axis',(0.,-1.,0.));
#7755=DIRECTION('ref_axis',(0.,0.,-1.));
#7756=DIRECTION('center_axis',(0.866025403784439,0.,-0.5));
#7757=DIRECTION('ref_axis',(0.5,0.,0.866025403784439));
#7758=DIRECTION('',(-0.5,0.,-0.866025403784439));
#7759=DIRECTION('',(0.,-1.,0.));
#7760=DIRECTION('',(0.5,0.,0.866025403784439));
#7761=DIRECTION('',(0.,-1.,0.));
#7762=DIRECTION('center_axis',(1.60246890531964E-16,0.,-1.));
#7763=DIRECTION('ref_axis',(1.,0.,1.60246890531964E-16));
#7764=DIRECTION('',(-1.,0.,-1.60246890531964E-16));
#7765=DIRECTION('',(0.,-1.,0.));
#7766=DIRECTION('',(1.,0.,1.60246890531964E-16));
#7767=DIRECTION('center_axis',(-0.866025403784439,0.,-0.5));
#7768=DIRECTION('ref_axis',(0.5,0.,-0.866025403784439));
#7769=DIRECTION('',(-0.5,0.,0.866025403784439));
#7770=DIRECTION('',(0.,-1.,0.));
#7771=DIRECTION('',(0.5,0.,-0.866025403784439));
#7772=DIRECTION('center_axis',(-0.866025403784439,0.,0.5));
#7773=DIRECTION('ref_axis',(-0.5,0.,-0.866025403784439));
#7774=DIRECTION('',(0.5,0.,0.866025403784439));
#7775=DIRECTION('',(0.,-1.,0.));
#7776=DIRECTION('',(-0.5,0.,-0.866025403784439));
#7777=DIRECTION('center_axis',(-1.60246890531964E-16,0.,1.));
#7778=DIRECTION('ref_axis',(-1.,0.,-1.60246890531964E-16));
#7779=DIRECTION('',(1.,0.,1.60246890531964E-16));
#7780=DIRECTION('',(0.,-1.,0.));
#7781=DIRECTION('',(-1.,0.,-1.60246890531964E-16));
#7782=DIRECTION('center_axis',(0.866025403784439,0.,0.5));
#7783=DIRECTION('ref_axis',(-0.5,0.,0.866025403784439));
#7784=DIRECTION('',(0.5,0.,-0.866025403784439));
#7785=DIRECTION('',(-0.5,0.,0.866025403784439));
#7786=DIRECTION('center_axis',(0.,1.,0.));
#7787=DIRECTION('ref_axis',(1.,0.,0.));
#7788=DIRECTION('center_axis',(0.,-1.,0.));
#7789=DIRECTION('ref_axis',(0.,0.,-1.));
#9924=CARTESIAN_POINT('',(0.,0.,0.));
#9925=CARTESIAN_POINT('Origin',(0.3,0.4,0.));
#9926=CARTESIAN_POINT('',(-0.3,0.4,-3.67394039744206E-17));
#9927=CARTESIAN_POINT('Origin',(0.,0.4,0.));
#9928=CARTESIAN_POINT('Origin',(0.,0.375,0.));
#9929=CARTESIAN_POINT('',(-0.35,0.35,-4.28626379701573E-17));
#9930=CARTESIAN_POINT('Origin',(0.,0.35,0.));
#9931=CARTESIAN_POINT('',(-0.325,0.375,-3.9801020972289E-17));
#9932=CARTESIAN_POINT('Origin',(0.,0.19,0.));
#9933=CARTESIAN_POINT('',(-0.35,0.03,-4.28626379701574E-17));
#9934=CARTESIAN_POINT('Origin',(0.,0.03,0.));
#9935=CARTESIAN_POINT('',(-0.35,0.19,-4.28626379701574E-17));
#9936=CARTESIAN_POINT('Origin',(0.,0.0149999999999999,0.));
#9937=CARTESIAN_POINT('',(-0.32,-3.29597460435593E-17,-3.91886975727153E-17));
#9938=CARTESIAN_POINT('Origin',(0.,0.,0.));
#9939=CARTESIAN_POINT('',(-0.335,0.0149999999999999,-4.10256677714363E-17));
#9940=CARTESIAN_POINT('Origin',(0.22,0.,0.));
#9941=CARTESIAN_POINT('',(-0.22,-6.93889390390723E-18,-2.69422295812418E-17));
#9942=CARTESIAN_POINT('Origin',(0.,0.,0.));
#9943=CARTESIAN_POINT('Origin',(0.,-0.02,0.));
#9944=CARTESIAN_POINT('',(-0.1954,-0.0492,2.39295984553393E-17));
#9945=CARTESIAN_POINT('Origin',(0.,-0.0492,0.));
#9946=CARTESIAN_POINT('',(-0.21,-0.02,-2.57175827820944E-17));
#9947=CARTESIAN_POINT('Origin',(0.,-0.8,0.));
#9948=CARTESIAN_POINT('',(-0.1954,-1.5646,2.39295984553393E-17));
#9949=CARTESIAN_POINT('Origin',(0.,-1.5646,0.));
#9950=CARTESIAN_POINT('',(-0.1954,-0.8,-2.39295984553393E-17));
#9951=CARTESIAN_POINT('Origin',(0.,-1.58,0.));
#9952=CARTESIAN_POINT('',(-0.16,-1.6,-1.95943487863577E-17));
#9953=CARTESIAN_POINT('Origin',(0.,-1.6,0.));
#9954=CARTESIAN_POINT('',(-0.18,-1.58,-2.20436423846524E-17));
#9955=CARTESIAN_POINT('Origin',(0.,-1.6,0.));
#9956=CARTESIAN_POINT('Origin',(0.0866025403784439,-0.4,-0.15));
#9957=CARTESIAN_POINT('',(0.173205080756888,-0.4,0.));
#9958=CARTESIAN_POINT('',(0.0866025403784439,-0.4,-0.15));
#9959=CARTESIAN_POINT('',(0.173205080756888,-0.4,0.));
#9960=CARTESIAN_POINT('',(0.0866025403784439,-0.64,-0.15));
#9961=CARTESIAN_POINT('',(0.0866025403784439,-0.4,-0.15));
#9962=CARTESIAN_POINT('',(0.173205080756888,-0.64,0.));
#9963=CARTESIAN_POINT('',(0.173205080756888,-0.64,0.));
#9964=CARTESIAN_POINT('',(0.173205080756888,-0.4,0.));
#9965=CARTESIAN_POINT('Origin',(-0.0866025403784438,-0.4,-0.15));
#9966=CARTESIAN_POINT('',(-0.0866025403784438,-0.4,-0.15));
#9967=CARTESIAN_POINT('',(0.0866025403784439,-0.4,-0.15));
#9968=CARTESIAN_POINT('',(-0.0866025403784438,-0.64,-0.15));
#9969=CARTESIAN_POINT('',(-0.0866025403784438,-0.4,-0.15));
#9970=CARTESIAN_POINT('',(0.0866025403784439,-0.64,-0.15));
#9971=CARTESIAN_POINT('Origin',(-0.173205080756888,-0.4,-2.77555756156289E-17));
#9972=CARTESIAN_POINT('',(-0.173205080756888,-0.4,-2.12115047744981E-17));
#9973=CARTESIAN_POINT('',(-0.0866025403784438,-0.4,-0.15));
#9974=CARTESIAN_POINT('',(-0.173205080756888,-0.64,-2.77555756156289E-17));
#9975=CARTESIAN_POINT('',(-0.173205080756888,-0.4,-2.12115047744981E-17));
#9976=CARTESIAN_POINT('',(-0.0866025403784438,-0.64,-0.15));
#9977=CARTESIAN_POINT('Origin',(-0.0866025403784439,-0.4,0.15));
#9978=CARTESIAN_POINT('',(-0.0866025403784439,-0.4,0.15));
#9979=CARTESIAN_POINT('',(-0.173205080756888,-0.4,-2.12115047744981E-17));
#9980=CARTESIAN_POINT('',(-0.0866025403784439,-0.64,0.15));
#9981=CARTESIAN_POINT('',(-0.0866025403784439,-0.4,0.15));
#9982=CARTESIAN_POINT('',(-0.173205080756888,-0.64,-2.12115047744981E-17));
#9983=CARTESIAN_POINT('Origin',(0.0866025403784439,-0.4,0.15));
#9984=CARTESIAN_POINT('',(0.0866025403784439,-0.4,0.15));
#9985=CARTESIAN_POINT('',(-0.0866025403784439,-0.4,0.15));
#9986=CARTESIAN_POINT('',(0.0866025403784439,-0.64,0.15));
#9987=CARTESIAN_POINT('',(0.0866025403784439,-0.4,0.15));
#9988=CARTESIAN_POINT('',(-0.0866025403784439,-0.64,0.15));
#9989=CARTESIAN_POINT('Origin',(0.173205080756888,-0.4,0.));
#9990=CARTESIAN_POINT('',(0.0866025403784439,-0.4,0.15));
#9991=CARTESIAN_POINT('',(0.0866025403784439,-0.64,0.15));
#9992=CARTESIAN_POINT('Origin',(0.,-0.4,-2.77555756156289E-17));
#9993=CARTESIAN_POINT('Origin',(0.,-0.64,-2.77555756156289E-17));
#10593=UNCERTAINTY_MEASURE_WITH_UNIT(LENGTH_MEASURE(0.001),#10651,
'DISTANCE_ACCURACY_VALUE',
'Maximum model space distance between geometric entities at asserted c
onnectivities');
#10611=UNCERTAINTY_MEASURE_WITH_UNIT(LENGTH_MEASURE(0.001),#10651,
'DISTANCE_ACCURACY_VALUE',
'Maximum model space distance between geometric entities at asserted c
onnectivities');
#10632=(
GEOMETRIC_REPRESENTATION_CONTEXT(3)
GLOBAL_UNCERTAINTY_ASSIGNED_CONTEXT((#10593))
GLOBAL_UNIT_ASSIGNED_CONTEXT((#10651,#10653,#10654))
REPRESENTATION_CONTEXT('','3D')
);
#10650=(
GEOMETRIC_REPRESENTATION_CONTEXT(3)
GLOBAL_UNCERTAINTY_ASSIGNED_CONTEXT((#10611))
GLOBAL_UNIT_ASSIGNED_CONTEXT((#10651,#10653,#10654))
REPRESENTATION_CONTEXT('','3D')
);
#10651=(
LENGTH_UNIT()
NAMED_UNIT(*)
SI_UNIT(.CENTI.,.METRE.)
);
#10653=(
NAMED_UNIT(*)
PLANE_ANGLE_UNIT()
SI_UNIT($,.RADIAN.)
);
#10654=(
NAMED_UNIT(*)
SI_UNIT($,.STERADIAN.)
SOLID_ANGLE_UNIT()
);
#10675=SHAPE_DEFINITION_REPRESENTATION(#10718,#10814);
#10718=PRODUCT_DEFINITION_SHAPE('',$,#10853);
#10814=SHAPE_REPRESENTATION('',(#6350),#10632);
#10832=PRODUCT_DEFINITION_CONTEXT('part definition',#10948,'design');
#10853=PRODUCT_DEFINITION('Cap Screw - M4x16','Cap Screw - M4x16',#10891,
#10832);
#10891=PRODUCT_DEFINITION_FORMATION('',$,#10970);
#10948=APPLICATION_CONTEXT(
'Core Data for Automotive Mechanical Design Process');
#10949=PRODUCT_CONTEXT('part definition',#10948,'mechanical');
#10970=PRODUCT('Cap Screw - M4x16','Cap Screw - M4x16',
'Cap Screw - M4x16',(#10949));
#11065=COLOUR_RGB('Black',0.12,0.14,0.17);
#11066=FILL_AREA_STYLE_COLOUR('',#11065);
#11067=FILL_AREA_STYLE('',(#11066));
#11068=SURFACE_STYLE_FILL_AREA(#11067);
#11069=SURFACE_SIDE_STYLE('',(#11068));
#11070=SURFACE_STYLE_USAGE(.BOTH.,#11069);
#11071=PRESENTATION_STYLE_ASSIGNMENT((#11070));
ENDSEC;
END-ISO-10303-21;
